ISO-10303-21;
HEADER;
/* Generated by software containing ST-Developer
 * from STEP Tools, Inc. (www.steptools.com) 
 */

FILE_DESCRIPTION(
/* description */ ('STEP AP214'),
/* implementation_level */ '2;1');

FILE_NAME(
/* name */ 'PRT-TQ-1012-12.step',
/* time_stamp */ '2026-10-07T12:49:37-07:00',
/* author */ (''),
/* organization */ (''),
/* preprocessor_version */ 'ST-DEVELOPER v20.2',
/* originating_system */ 'Autodesk Translation Framework v15.15.0.0',
/* authorisation */ '');

FILE_SCHEMA (('AUTOMOTIVE_DESIGN { 1 0 10303 214 3 1 1 }'));
ENDSEC;

DATA;
#10=MECHANICAL_DESIGN_GEOMETRIC_PRESENTATION_REPRESENTATION('',(#297),#33016);
#243=SHAPE_REPRESENTATION_RELATIONSHIP('SRR','None',#33137,#270);
#270=ADVANCED_BREP_SHAPE_REPRESENTATION('',(#328),#32998);
#297=STYLED_ITEM('',(#33288),#328);
#328=MANIFOLD_SOLID_BREP('Body1',#9952);
#511=FACE_BOUND('',#1912,.T.);
#512=FACE_BOUND('',#1914,.T.);
#513=FACE_BOUND('',#1916,.T.);
#631=B_SPLINE_CURVE_WITH_KNOTS('',3,(#23782,#23783,#23784,#23785,#23786,
#23787,#23788,#23789,#23790,#23791),.UNSPECIFIED.,.F.,.F.,(4,2,2,2,4),(-0.321465265823507,
-0.241103193298965,-0.160741120774423,-0.0803705603872117,0.),
 .UNSPECIFIED.);
#632=B_SPLINE_CURVE_WITH_KNOTS('',3,(#23793,#23794,#23795,#23796,#23797,
#23798,#23799,#23800,#23801,#23802),.UNSPECIFIED.,.F.,.F.,(4,2,2,2,4),(0.,
0.0803705603872116,0.160741120774423,0.241103193298965,0.321465265823507),
 .UNSPECIFIED.);
#633=B_SPLINE_CURVE_WITH_KNOTS('',3,(#23807,#23808,#23809,#23810,#23811,
#23812,#23813,#23814,#23815,#23816),.UNSPECIFIED.,.F.,.F.,(4,2,2,2,4),(0.321465265823507,
0.401827338348048,0.48218941087259,0.562559971259802,0.642930531647013),
 .UNSPECIFIED.);
#634=B_SPLINE_CURVE_WITH_KNOTS('',3,(#23817,#23818,#23819,#23820,#23821,
#23822,#23823,#23824,#23825,#23826),.UNSPECIFIED.,.F.,.F.,(4,2,2,2,4),(-0.642930531647014,
-0.562559971259802,-0.48218941087259,-0.401827338348049,-0.321465265823507),
 .UNSPECIFIED.);
#635=B_SPLINE_CURVE_WITH_KNOTS('',3,(#23829,#23830,#23831,#23832,#23833,
#23834,#23835,#23836,#23837,#23838),.UNSPECIFIED.,.F.,.F.,(4,2,2,2,4),(0.96439579747052,
1.04475786999506,1.1251199425196,1.20549050290682,1.28586106329403),
 .UNSPECIFIED.);
#636=B_SPLINE_CURVE_WITH_KNOTS('',3,(#23839,#23840,#23841,#23842,#23843,
#23844,#23845,#23846,#23847,#23848,#23849,#23850,#23851,#23852,#23853,#23854,
#23855,#23856,#23857,#23858,#23859,#23860,#23861,#23862,#23863,#23864),
 .UNSPECIFIED.,.F.,.F.,(4,2,2,2,2,2,2,2,2,2,2,2,4),(1.28586106329403,1.36623162368124,
1.44660218406845,1.52696425659299,1.60732632911753,1.68768840164208,1.76805047416662,
1.84842103455383,1.92879159494104,2.00916215532825,2.08953271571546,2.16989478824001,
2.25025686076455),.UNSPECIFIED.);
#900=PLANE('',#10771);
#901=PLANE('',#10773);
#902=PLANE('',#10777);
#903=PLANE('',#10780);
#1318=FACE_OUTER_BOUND('',#1911,.T.);
#1319=FACE_OUTER_BOUND('',#1913,.T.);
#1320=FACE_OUTER_BOUND('',#1915,.T.);
#1321=FACE_OUTER_BOUND('',#1917,.T.);
#1322=FACE_OUTER_BOUND('',#1918,.T.);
#1323=FACE_OUTER_BOUND('',#1919,.T.);
#1324=FACE_OUTER_BOUND('',#1920,.T.);
#1325=FACE_OUTER_BOUND('',#1921,.T.);
#1911=EDGE_LOOP('',(#7974,#7975,#7976,#7977,#7978,#7979,#7980,#7981,#7982,
#7983));
#1912=EDGE_LOOP('',(#7984,#7985));
#1913=EDGE_LOOP('',(#7986));
#1914=EDGE_LOOP('',(#7987));
#1915=EDGE_LOOP('',(#7988));
#1916=EDGE_LOOP('',(#7989));
#1917=EDGE_LOOP('',(#7990,#7991,#7992,#7993,#7994,#7995,#7996));
#1918=EDGE_LOOP('',(#7997));
#1919=EDGE_LOOP('',(#7998,#7999,#8000,#8001,#8002));
#1920=EDGE_LOOP('',(#8003));
#1921=EDGE_LOOP('',(#8004,#8005,#8006,#8007));
#2434=CIRCLE('',#10769,9.1);
#2435=CIRCLE('',#10770,9.1);
#2436=CIRCLE('',#10772,3.5);
#2437=CIRCLE('',#10774,3.5);
#2438=CIRCLE('',#10776,2.125);
#2439=CIRCLE('',#10779,2.125);
#3051=LINE('',#23780,#3801);
#3052=LINE('',#23804,#3802);
#3053=LINE('',#23874,#3803);
#3054=LINE('',#23879,#3804);
#3055=LINE('',#23882,#3805);
#3801=VECTOR('',#12690,9.1);
#3802=VECTOR('',#12691,9.1);
#3803=VECTOR('',#12706,2.125);
#3804=VECTOR('',#12713,2.125);
#3805=VECTOR('',#12718,3.5);
#4608=VERTEX_POINT('',#23777);
#4609=VERTEX_POINT('',#23779);
#4610=VERTEX_POINT('',#23781);
#4611=VERTEX_POINT('',#23792);
#4612=VERTEX_POINT('',#23803);
#4613=VERTEX_POINT('',#23806);
#4614=VERTEX_POINT('',#23827);
#4615=VERTEX_POINT('',#23828);
#4616=VERTEX_POINT('',#23866);
#4617=VERTEX_POINT('',#23869);
#4618=VERTEX_POINT('',#23872);
#4619=VERTEX_POINT('',#23877);
#5800=EDGE_CURVE('',#4608,#4608,#2434,.T.);
#5801=EDGE_CURVE('',#4608,#4609,#3051,.T.);
#5802=EDGE_CURVE('',#4609,#4610,#631,.T.);
#5803=EDGE_CURVE('',#4610,#4611,#632,.T.);
#5804=EDGE_CURVE('',#4611,#4612,#3052,.T.);
#5805=EDGE_CURVE('',#4612,#4612,#2435,.T.);
#5806=EDGE_CURVE('',#4611,#4613,#633,.T.);
#5807=EDGE_CURVE('',#4613,#4609,#634,.T.);
#5808=EDGE_CURVE('',#4614,#4615,#635,.T.);
#5809=EDGE_CURVE('',#4615,#4614,#636,.T.);
#5810=EDGE_CURVE('',#4616,#4616,#2436,.T.);
#5811=EDGE_CURVE('',#4617,#4617,#2437,.T.);
#5812=EDGE_CURVE('',#4618,#4618,#2438,.T.);
#5813=EDGE_CURVE('',#4618,#4610,#3053,.T.);
#5814=EDGE_CURVE('',#4619,#4619,#2439,.T.);
#5815=EDGE_CURVE('',#4619,#4615,#3054,.T.);
#5816=EDGE_CURVE('',#4616,#4617,#3055,.T.);
#7974=ORIENTED_EDGE('',*,*,#5800,.T.);
#7975=ORIENTED_EDGE('',*,*,#5801,.T.);
#7976=ORIENTED_EDGE('',*,*,#5802,.T.);
#7977=ORIENTED_EDGE('',*,*,#5803,.T.);
#7978=ORIENTED_EDGE('',*,*,#5804,.T.);
#7979=ORIENTED_EDGE('',*,*,#5805,.F.);
#7980=ORIENTED_EDGE('',*,*,#5804,.F.);
#7981=ORIENTED_EDGE('',*,*,#5806,.T.);
#7982=ORIENTED_EDGE('',*,*,#5807,.T.);
#7983=ORIENTED_EDGE('',*,*,#5801,.F.);
#7984=ORIENTED_EDGE('',*,*,#5808,.F.);
#7985=ORIENTED_EDGE('',*,*,#5809,.F.);
#7986=ORIENTED_EDGE('',*,*,#5805,.T.);
#7987=ORIENTED_EDGE('',*,*,#5810,.F.);
#7988=ORIENTED_EDGE('',*,*,#5800,.F.);
#7989=ORIENTED_EDGE('',*,*,#5811,.F.);
#7990=ORIENTED_EDGE('',*,*,#5812,.F.);
#7991=ORIENTED_EDGE('',*,*,#5813,.T.);
#7992=ORIENTED_EDGE('',*,*,#5802,.F.);
#7993=ORIENTED_EDGE('',*,*,#5807,.F.);
#7994=ORIENTED_EDGE('',*,*,#5806,.F.);
#7995=ORIENTED_EDGE('',*,*,#5803,.F.);
#7996=ORIENTED_EDGE('',*,*,#5813,.F.);
#7997=ORIENTED_EDGE('',*,*,#5812,.T.);
#7998=ORIENTED_EDGE('',*,*,#5814,.T.);
#7999=ORIENTED_EDGE('',*,*,#5815,.T.);
#8000=ORIENTED_EDGE('',*,*,#5809,.T.);
#8001=ORIENTED_EDGE('',*,*,#5808,.T.);
#8002=ORIENTED_EDGE('',*,*,#5815,.F.);
#8003=ORIENTED_EDGE('',*,*,#5814,.F.);
#8004=ORIENTED_EDGE('',*,*,#5810,.T.);
#8005=ORIENTED_EDGE('',*,*,#5816,.T.);
#8006=ORIENTED_EDGE('',*,*,#5811,.T.);
#8007=ORIENTED_EDGE('',*,*,#5816,.F.);
#9307=CYLINDRICAL_SURFACE('',#10768,9.1);
#9308=CYLINDRICAL_SURFACE('',#10775,2.125);
#9309=CYLINDRICAL_SURFACE('',#10778,2.125);
#9310=CYLINDRICAL_SURFACE('',#10781,3.5);
#9684=ADVANCED_FACE('',(#1318,#511),#9307,.T.);
#9685=ADVANCED_FACE('',(#1319,#512),#900,.T.);
#9686=ADVANCED_FACE('',(#1320,#513),#901,.F.);
#9687=ADVANCED_FACE('',(#1321),#9308,.F.);
#9688=ADVANCED_FACE('',(#1322),#902,.T.);
#9689=ADVANCED_FACE('',(#1323),#9309,.F.);
#9690=ADVANCED_FACE('',(#1324),#903,.T.);
#9691=ADVANCED_FACE('',(#1325),#9310,.F.);
#9952=CLOSED_SHELL('',(#9684,#9685,#9686,#9687,#9688,#9689,#9690,#9691));
#10767=AXIS2_PLACEMENT_3D('',#23775,#12684,#12685);
#10768=AXIS2_PLACEMENT_3D('',#23776,#12686,#12687);
#10769=AXIS2_PLACEMENT_3D('',#23778,#12688,#12689);
#10770=AXIS2_PLACEMENT_3D('',#23805,#12692,#12693);
#10771=AXIS2_PLACEMENT_3D('',#23865,#12694,#12695);
#10772=AXIS2_PLACEMENT_3D('',#23867,#12696,#12697);
#10773=AXIS2_PLACEMENT_3D('',#23868,#12698,#12699);
#10774=AXIS2_PLACEMENT_3D('',#23870,#12700,#12701);
#10775=AXIS2_PLACEMENT_3D('',#23871,#12702,#12703);
#10776=AXIS2_PLACEMENT_3D('',#23873,#12704,#12705);
#10777=AXIS2_PLACEMENT_3D('',#23875,#12707,#12708);
#10778=AXIS2_PLACEMENT_3D('',#23876,#12709,#12710);
#10779=AXIS2_PLACEMENT_3D('',#23878,#12711,#12712);
#10780=AXIS2_PLACEMENT_3D('',#23880,#12714,#12715);
#10781=AXIS2_PLACEMENT_3D('',#23881,#12716,#12717);
#12684=DIRECTION('axis',(0.,0.,1.));
#12685=DIRECTION('refdir',(1.,0.,0.));
#12686=DIRECTION('center_axis',(0.,-1.,0.));
#12687=DIRECTION('ref_axis',(0.,0.,-1.));
#12688=DIRECTION('center_axis',(0.,1.,0.));
#12689=DIRECTION('ref_axis',(0.,0.,1.));
#12690=DIRECTION('',(0.,1.,0.));
#12691=DIRECTION('',(0.,1.,0.));
#12692=DIRECTION('center_axis',(0.,1.,0.));
#12693=DIRECTION('ref_axis',(0.,0.,1.));
#12694=DIRECTION('center_axis',(0.,1.,0.));
#12695=DIRECTION('ref_axis',(0.,0.,1.));
#12696=DIRECTION('center_axis',(0.,1.,0.));
#12697=DIRECTION('ref_axis',(0.,0.,1.));
#12698=DIRECTION('center_axis',(0.,1.,0.));
#12699=DIRECTION('ref_axis',(0.,0.,1.));
#12700=DIRECTION('center_axis',(0.,-1.,0.));
#12701=DIRECTION('ref_axis',(0.,0.,-1.));
#12702=DIRECTION('center_axis',(0.,0.,1.));
#12703=DIRECTION('ref_axis',(1.,0.,0.));
#12704=DIRECTION('center_axis',(0.,0.,1.));
#12705=DIRECTION('ref_axis',(1.,0.,0.));
#12706=DIRECTION('',(0.,0.,1.));
#12707=DIRECTION('center_axis',(0.,0.,1.));
#12708=DIRECTION('ref_axis',(1.,0.,0.));
#12709=DIRECTION('center_axis',(0.,0.,-1.));
#12710=DIRECTION('ref_axis',(-1.,0.,0.));
#12711=DIRECTION('center_axis',(0.,0.,1.));
#12712=DIRECTION('ref_axis',(1.,0.,0.));
#12713=DIRECTION('',(0.,0.,-1.));
#12714=DIRECTION('center_axis',(0.,0.,-1.));
#12715=DIRECTION('ref_axis',(1.,0.,0.));
#12716=DIRECTION('center_axis',(0.,-1.,0.));
#12717=DIRECTION('ref_axis',(0.,0.,-1.));
#12718=DIRECTION('',(0.,-1.,0.));
#23775=CARTESIAN_POINT('',(0.,0.,0.));
#23776=CARTESIAN_POINT('Origin',(0.,10.,0.));
#23777=CARTESIAN_POINT('',(0.,0.,9.1));
#23778=CARTESIAN_POINT('Origin',(0.,0.,0.));
#23779=CARTESIAN_POINT('',(-4.87825354572973E-16,2.875,9.1));
#23780=CARTESIAN_POINT('',(-1.11442858722409E-15,10.,9.1));
#23781=CARTESIAN_POINT('',(-2.125,5.,8.84841087427567));
#23782=CARTESIAN_POINT('Ctrl Pts',(1.38777878078145E-16,2.875,9.1));
#23783=CARTESIAN_POINT('Ctrl Pts',(-0.267873575081806,2.875,9.1));
#23784=CARTESIAN_POINT('Ctrl Pts',(-0.5529354090087,2.92873648721047,9.08698350329319));
#23785=CARTESIAN_POINT('Ctrl Pts',(-1.07620906803504,3.145911519284,9.03995469026056));
#23786=CARTESIAN_POINT('Ctrl Pts',(-1.31450018724633,3.3092963672035,9.00657888722713));
#23787=CARTESIAN_POINT('Ctrl Pts',(-1.69072350014861,3.68551968010578,8.94359188045991));
#23788=CARTESIAN_POINT('Ctrl Pts',(-1.85409283030911,3.92380246738359,8.9098094730266));
#23789=CARTESIAN_POINT('Ctrl Pts',(-2.0712565629818,4.44704679048386,8.86184301458953));
#23790=CARTESIAN_POINT('Ctrl Pts',(-2.125,4.73209813204263,8.84841087427567));
#23791=CARTESIAN_POINT('Ctrl Pts',(-2.125,5.,8.84841087427567));
#23792=CARTESIAN_POINT('',(-5.2251982409251E-16,7.125,9.1));
#23793=CARTESIAN_POINT('Ctrl Pts',(-2.125,5.,8.84841087427567));
#23794=CARTESIAN_POINT('Ctrl Pts',(-2.125,5.26790186795737,8.84841087427567));
#23795=CARTESIAN_POINT('Ctrl Pts',(-2.0712565629818,5.55295320951614,8.86184301458953));
#23796=CARTESIAN_POINT('Ctrl Pts',(-1.85409283030911,6.07619753261641,8.9098094730266));
#23797=CARTESIAN_POINT('Ctrl Pts',(-1.69072350014861,6.31448031989422,8.94359188045991));
#23798=CARTESIAN_POINT('Ctrl Pts',(-1.31450018724633,6.6907036327965,9.00657888722713));
#23799=CARTESIAN_POINT('Ctrl Pts',(-1.07620906803504,6.854088480716,9.03995469026056));
#23800=CARTESIAN_POINT('Ctrl Pts',(-0.552935409008698,7.07126351278953,
9.08698350329319));
#23801=CARTESIAN_POINT('Ctrl Pts',(-0.267873575081805,7.125,9.1));
#23802=CARTESIAN_POINT('Ctrl Pts',(3.46944695195361E-16,7.125,9.1));
#23803=CARTESIAN_POINT('',(0.,10.,9.1));
#23804=CARTESIAN_POINT('',(-1.11442858722409E-15,10.,9.1));
#23805=CARTESIAN_POINT('Origin',(0.,10.,0.));
#23806=CARTESIAN_POINT('',(2.125,5.,8.84841087427567));
#23807=CARTESIAN_POINT('Ctrl Pts',(2.77555756156289E-16,7.125,9.1));
#23808=CARTESIAN_POINT('Ctrl Pts',(0.267873575081806,7.125,9.1));
#23809=CARTESIAN_POINT('Ctrl Pts',(0.5529354090087,7.07126351278953,9.08698350329319));
#23810=CARTESIAN_POINT('Ctrl Pts',(1.07620906803504,6.854088480716,9.03995469026056));
#23811=CARTESIAN_POINT('Ctrl Pts',(1.31450018724633,6.6907036327965,9.00657888722713));
#23812=CARTESIAN_POINT('Ctrl Pts',(1.69072350014861,6.31448031989422,8.94359188045991));
#23813=CARTESIAN_POINT('Ctrl Pts',(1.85409283030911,6.07619753261641,8.9098094730266));
#23814=CARTESIAN_POINT('Ctrl Pts',(2.0712565629818,5.55295320951614,8.86184301458953));
#23815=CARTESIAN_POINT('Ctrl Pts',(2.125,5.26790186795737,8.84841087427567));
#23816=CARTESIAN_POINT('Ctrl Pts',(2.125,5.,8.84841087427567));
#23817=CARTESIAN_POINT('Ctrl Pts',(2.125,5.,8.84841087427567));
#23818=CARTESIAN_POINT('Ctrl Pts',(2.125,4.73209813204263,8.84841087427567));
#23819=CARTESIAN_POINT('Ctrl Pts',(2.0712565629818,4.44704679048386,8.86184301458953));
#23820=CARTESIAN_POINT('Ctrl Pts',(1.85409283030911,3.92380246738359,8.9098094730266));
#23821=CARTESIAN_POINT('Ctrl Pts',(1.69072350014861,3.68551968010578,8.94359188045991));
#23822=CARTESIAN_POINT('Ctrl Pts',(1.31450018724633,3.3092963672035,9.00657888722713));
#23823=CARTESIAN_POINT('Ctrl Pts',(1.07620906803504,3.145911519284,9.03995469026056));
#23824=CARTESIAN_POINT('Ctrl Pts',(0.552935409008699,2.92873648721047,9.08698350329319));
#23825=CARTESIAN_POINT('Ctrl Pts',(0.267873575081806,2.875,9.1));
#23826=CARTESIAN_POINT('Ctrl Pts',(1.38777878078145E-16,2.875,9.1));
#23827=CARTESIAN_POINT('',(0.,7.125,-9.1));
#23828=CARTESIAN_POINT('',(2.125,5.,-8.84841087427567));
#23829=CARTESIAN_POINT('Ctrl Pts',(-1.38777878078145E-16,7.125,-9.1));
#23830=CARTESIAN_POINT('Ctrl Pts',(0.267873575081805,7.125,-9.1));
#23831=CARTESIAN_POINT('Ctrl Pts',(0.552935409008698,7.07126351278953,-9.08698350329319));
#23832=CARTESIAN_POINT('Ctrl Pts',(1.07620906803504,6.854088480716,-9.03995469026056));
#23833=CARTESIAN_POINT('Ctrl Pts',(1.31450018724633,6.6907036327965,-9.00657888722713));
#23834=CARTESIAN_POINT('Ctrl Pts',(1.69072350014861,6.31448031989422,-8.94359188045991));
#23835=CARTESIAN_POINT('Ctrl Pts',(1.85409283030911,6.07619753261641,-8.9098094730266));
#23836=CARTESIAN_POINT('Ctrl Pts',(2.0712565629818,5.55295320951614,-8.86184301458953));
#23837=CARTESIAN_POINT('Ctrl Pts',(2.125,5.26790186795737,-8.84841087427567));
#23838=CARTESIAN_POINT('Ctrl Pts',(2.125,5.,-8.84841087427567));
#23839=CARTESIAN_POINT('Ctrl Pts',(2.125,5.,-8.84841087427567));
#23840=CARTESIAN_POINT('Ctrl Pts',(2.125,4.73209813204263,-8.84841087427567));
#23841=CARTESIAN_POINT('Ctrl Pts',(2.0712565629818,4.44704679048386,-8.86184301458953));
#23842=CARTESIAN_POINT('Ctrl Pts',(1.85409283030911,3.92380246738359,-8.9098094730266));
#23843=CARTESIAN_POINT('Ctrl Pts',(1.69072350014861,3.68551968010578,-8.94359188045991));
#23844=CARTESIAN_POINT('Ctrl Pts',(1.31450018724633,3.3092963672035,-9.00657888722713));
#23845=CARTESIAN_POINT('Ctrl Pts',(1.07620906803504,3.145911519284,-9.03995469026056));
#23846=CARTESIAN_POINT('Ctrl Pts',(0.5529354090087,2.92873648721047,-9.08698350329319));
#23847=CARTESIAN_POINT('Ctrl Pts',(0.267873575081805,2.875,-9.1));
#23848=CARTESIAN_POINT('Ctrl Pts',(-0.267873575081806,2.875,-9.1));
#23849=CARTESIAN_POINT('Ctrl Pts',(-0.552935409008699,2.92873648721047,
-9.08698350329319));
#23850=CARTESIAN_POINT('Ctrl Pts',(-1.07620906803504,3.145911519284,-9.03995469026056));
#23851=CARTESIAN_POINT('Ctrl Pts',(-1.31450018724633,3.3092963672035,-9.00657888722713));
#23852=CARTESIAN_POINT('Ctrl Pts',(-1.69072350014861,3.68551968010578,-8.94359188045991));
#23853=CARTESIAN_POINT('Ctrl Pts',(-1.85409283030911,3.92380246738359,-8.9098094730266));
#23854=CARTESIAN_POINT('Ctrl Pts',(-2.0712565629818,4.44704679048386,-8.86184301458953));
#23855=CARTESIAN_POINT('Ctrl Pts',(-2.125,4.73209813204263,-8.84841087427567));
#23856=CARTESIAN_POINT('Ctrl Pts',(-2.125,5.26790186795737,-8.84841087427567));
#23857=CARTESIAN_POINT('Ctrl Pts',(-2.0712565629818,5.55295320951614,-8.86184301458953));
#23858=CARTESIAN_POINT('Ctrl Pts',(-1.85409283030911,6.07619753261641,-8.9098094730266));
#23859=CARTESIAN_POINT('Ctrl Pts',(-1.69072350014861,6.31448031989422,-8.94359188045991));
#23860=CARTESIAN_POINT('Ctrl Pts',(-1.31450018724633,6.6907036327965,-9.00657888722713));
#23861=CARTESIAN_POINT('Ctrl Pts',(-1.07620906803504,6.854088480716,-9.03995469026056));
#23862=CARTESIAN_POINT('Ctrl Pts',(-0.5529354090087,7.07126351278953,-9.08698350329319));
#23863=CARTESIAN_POINT('Ctrl Pts',(-0.267873575081806,7.125,-9.1));
#23864=CARTESIAN_POINT('Ctrl Pts',(-2.08166817117217E-16,7.125,-9.1));
#23865=CARTESIAN_POINT('Origin',(0.,10.,0.));
#23866=CARTESIAN_POINT('',(0.,10.,3.5));
#23867=CARTESIAN_POINT('Origin',(0.,10.,0.));
#23868=CARTESIAN_POINT('Origin',(0.,0.,0.));
#23869=CARTESIAN_POINT('',(-4.28626379701573E-16,1.22464679914735E-16,3.5));
#23870=CARTESIAN_POINT('Origin',(0.,1.22464679914735E-16,0.));
#23871=CARTESIAN_POINT('Origin',(0.,5.,6.1));
#23872=CARTESIAN_POINT('',(-2.125,5.,6.1));
#23873=CARTESIAN_POINT('Origin',(0.,5.,6.1));
#23874=CARTESIAN_POINT('',(-2.125,5.,6.1));
#23875=CARTESIAN_POINT('Origin',(0.,5.,6.1));
#23876=CARTESIAN_POINT('Origin',(0.,5.,-6.1));
#23877=CARTESIAN_POINT('',(2.125,5.,-6.1));
#23878=CARTESIAN_POINT('Origin',(0.,5.,-6.1));
#23879=CARTESIAN_POINT('',(2.125,5.,-6.1));
#23880=CARTESIAN_POINT('Origin',(0.,5.,-6.1));
#23881=CARTESIAN_POINT('Origin',(0.,0.,0.));
#23882=CARTESIAN_POINT('',(-4.28626379701573E-16,0.,3.5));
#32966=UNCERTAINTY_MEASURE_WITH_UNIT(LENGTH_MEASURE(0.01),#33017,
'DISTANCE_ACCURACY_VALUE',
'Maximum model space distance between geometric entities at asserted c
onnectivities');
#32984=UNCERTAINTY_MEASURE_WITH_UNIT(LENGTH_MEASURE(0.01),#33017,
'DISTANCE_ACCURACY_VALUE',
'Maximum model space distance between geometric entities at asserted c
onnectivities');
#32998=(
GEOMETRIC_REPRESENTATION_CONTEXT(3)
GLOBAL_UNCERTAINTY_ASSIGNED_CONTEXT((#32966))
GLOBAL_UNIT_ASSIGNED_CONTEXT((#33017,#33019,#33020))
REPRESENTATION_CONTEXT('','3D')
);
#33016=(
GEOMETRIC_REPRESENTATION_CONTEXT(3)
GLOBAL_UNCERTAINTY_ASSIGNED_CONTEXT((#32984))
GLOBAL_UNIT_ASSIGNED_CONTEXT((#33017,#33019,#33020))
REPRESENTATION_CONTEXT('','3D')
);
#33017=(
LENGTH_UNIT()
NAMED_UNIT(*)
SI_UNIT(.MILLI.,.METRE.)
);
#33019=(
NAMED_UNIT(*)
PLANE_ANGLE_UNIT()
SI_UNIT($,.RADIAN.)
);
#33020=(
NAMED_UNIT(*)
SI_UNIT($,.STERADIAN.)
SOLID_ANGLE_UNIT()
);
#33034=SHAPE_DEFINITION_REPRESENTATION(#33073,#33137);
#33073=PRODUCT_DEFINITION_SHAPE('',$,#33169);
#33137=SHAPE_REPRESENTATION('',(#10767),#32998);
#33155=PRODUCT_DEFINITION_CONTEXT('part definition',#33250,'design');
#33169=PRODUCT_DEFINITION(
'P_Torque Wrench_Barrel Nut_PRT-TQ-1012-12_M_Rev01','PRT-TQ-1012-12',#33200,
#33155);
#33200=PRODUCT_DEFINITION_FORMATION('',$,#33265);
#33250=APPLICATION_CONTEXT(
'Core Data for Automotive Mechanical Design Process');
#33251=PRODUCT_CONTEXT('part definition',#33250,'mechanical');
#33265=PRODUCT('P_Torque Wrench_Barrel Nut_PRT-TQ-1012-12_M_Rev01',
'PRT-TQ-1012-12',$,(#33251));
#33288=PRESENTATION_STYLE_ASSIGNMENT((#33295));
#33295=SURFACE_STYLE_USAGE(.BOTH.,#33302);
#33302=SURFACE_SIDE_STYLE('',(#33309));
#33309=SURFACE_STYLE_FILL_AREA(#33316);
#33316=FILL_AREA_STYLE('Opaque(192,192,192)',(#33323));
#33323=FILL_AREA_STYLE_COLOUR('Opaque(192,192,192)',#33330);
#33330=COLOUR_RGB('Opaque(192,192,192)', 0.72549020, 0.75294118, 0.79215686);
ENDSEC;
END-ISO-10303-21;
